ISO-10303-21;
HEADER;
/* Generated by software containing ST-Developer
 * from STEP Tools, Inc. (www.steptools.com) 
 */

FILE_DESCRIPTION(
/* description */ ('Five-roller gravity conveyor'),
/* implementation_level */ '2;1');

FILE_NAME(
/* name */ 'Bracket spacer.step',
/* time_stamp */ '2026-10-29T15:36:43-07:00',
/* author */ (''),
/* organization */ (''),
/* preprocessor_version */ 'ST-DEVELOPER v20.2',
/* originating_system */ 'Autodesk Translation Framework v15.17.0.0',
/* authorisation */ '');

FILE_SCHEMA (('AUTOMOTIVE_DESIGN { 1 0 10303 214 3 1 1 }'));
ENDSEC;

DATA;
#10=MECHANICAL_DESIGN_GEOMETRIC_PRESENTATION_REPRESENTATION('',(#333),#7806);
#289=SHAPE_REPRESENTATION_RELATIONSHIP('SRR','None',#7927,#307);
#307=ADVANCED_BREP_SHAPE_REPRESENTATION('',(#358),#7800);
#333=STYLED_ITEM('',(#8070),#358);
#358=MANIFOLD_SOLID_BREP('Body1',#4221);
#395=FACE_BOUND('',#1109,.T.);
#396=FACE_BOUND('',#1111,.T.);
#552=CIRCLE('',#4772,0.605);
#553=CIRCLE('',#4773,0.605);
#554=CIRCLE('',#4775,1.);
#555=CIRCLE('',#4776,1.);
#633=CYLINDRICAL_SURFACE('',#4771,0.605);
#634=CYLINDRICAL_SURFACE('',#4774,1.);
#841=FACE_OUTER_BOUND('',#1106,.T.);
#842=FACE_OUTER_BOUND('',#1107,.T.);
#843=FACE_OUTER_BOUND('',#1108,.T.);
#844=FACE_OUTER_BOUND('',#1110,.T.);
#1106=EDGE_LOOP('',(#3656,#3657,#3658,#3659));
#1107=EDGE_LOOP('',(#3660,#3661,#3662,#3663));
#1108=EDGE_LOOP('',(#3664));
#1109=EDGE_LOOP('',(#3665));
#1110=EDGE_LOOP('',(#3666));
#1111=EDGE_LOOP('',(#3667));
#1475=LINE('',#7530,#1816);
#1476=LINE('',#7536,#1817);
#1816=VECTOR('',#5903,0.605);
#1817=VECTOR('',#5910,1.);
#2166=VERTEX_POINT('',#7527);
#2167=VERTEX_POINT('',#7529);
#2168=VERTEX_POINT('',#7533);
#2169=VERTEX_POINT('',#7535);
#2671=EDGE_CURVE('',#2166,#2166,#552,.T.);
#2672=EDGE_CURVE('',#2166,#2167,#1475,.T.);
#2673=EDGE_CURVE('',#2167,#2167,#553,.T.);
#2674=EDGE_CURVE('',#2168,#2168,#554,.T.);
#2675=EDGE_CURVE('',#2168,#2169,#1476,.T.);
#2676=EDGE_CURVE('',#2169,#2169,#555,.T.);
#3656=ORIENTED_EDGE('',*,*,#2671,.F.);
#3657=ORIENTED_EDGE('',*,*,#2672,.T.);
#3658=ORIENTED_EDGE('',*,*,#2673,.T.);
#3659=ORIENTED_EDGE('',*,*,#2672,.F.);
#3660=ORIENTED_EDGE('',*,*,#2674,.F.);
#3661=ORIENTED_EDGE('',*,*,#2675,.T.);
#3662=ORIENTED_EDGE('',*,*,#2676,.T.);
#3663=ORIENTED_EDGE('',*,*,#2675,.F.);
#3664=ORIENTED_EDGE('',*,*,#2674,.T.);
#3665=ORIENTED_EDGE('',*,*,#2671,.T.);
#3666=ORIENTED_EDGE('',*,*,#2676,.F.);
#3667=ORIENTED_EDGE('',*,*,#2673,.F.);
#3947=PLANE('',#4777);
#3948=PLANE('',#4778);
#4156=ADVANCED_FACE('',(#841),#633,.F.);
#4157=ADVANCED_FACE('',(#842),#634,.T.);
#4158=ADVANCED_FACE('',(#843,#395),#3947,.T.);
#4159=ADVANCED_FACE('',(#844,#396),#3948,.F.);
#4221=CLOSED_SHELL('',(#4156,#4157,#4158,#4159));
#4770=AXIS2_PLACEMENT_3D('',#7525,#5897,#5898);
#4771=AXIS2_PLACEMENT_3D('',#7526,#5899,#5900);
#4772=AXIS2_PLACEMENT_3D('',#7528,#5901,#5902);
#4773=AXIS2_PLACEMENT_3D('',#7531,#5904,#5905);
#4774=AXIS2_PLACEMENT_3D('',#7532,#5906,#5907);
#4775=AXIS2_PLACEMENT_3D('',#7534,#5908,#5909);
#4776=AXIS2_PLACEMENT_3D('',#7537,#5911,#5912);
#4777=AXIS2_PLACEMENT_3D('',#7538,#5913,#5914);
#4778=AXIS2_PLACEMENT_3D('',#7539,#5915,#5916);
#5897=DIRECTION('axis',(0.,0.,1.));
#5898=DIRECTION('refdir',(1.,0.,0.));
#5899=DIRECTION('center_axis',(0.,1.,0.));
#5900=DIRECTION('ref_axis',(1.,0.,0.));
#5901=DIRECTION('center_axis',(0.,-1.,0.));
#5902=DIRECTION('ref_axis',(1.,0.,0.));
#5903=DIRECTION('',(0.,-1.,0.));
#5904=DIRECTION('center_axis',(0.,-1.,0.));
#5905=DIRECTION('ref_axis',(1.,0.,0.));
#5906=DIRECTION('center_axis',(0.,1.,0.));
#5907=DIRECTION('ref_axis',(1.,0.,0.));
#5908=DIRECTION('center_axis',(0.,1.,0.));
#5909=DIRECTION('ref_axis',(1.,0.,0.));
#5910=DIRECTION('',(0.,-1.,0.));
#5911=DIRECTION('center_axis',(0.,1.,0.));
#5912=DIRECTION('ref_axis',(1.,0.,0.));
#5913=DIRECTION('center_axis',(0.,1.,0.));
#5914=DIRECTION('ref_axis',(1.,0.,0.));
#5915=DIRECTION('center_axis',(0.,1.,0.));
#5916=DIRECTION('ref_axis',(1.,0.,0.));
#7525=CARTESIAN_POINT('',(0.,0.,0.));
#7526=CARTESIAN_POINT('Origin',(0.,-2.5,4.5));
#7527=CARTESIAN_POINT('',(-0.605,-2.4,4.5));
#7528=CARTESIAN_POINT('Origin',(0.,-2.4,4.5));
#7529=CARTESIAN_POINT('',(-0.605,-2.5,4.5));
#7530=CARTESIAN_POINT('',(-0.605,-2.5,4.5));
#7531=CARTESIAN_POINT('Origin',(0.,-2.5,4.5));
#7532=CARTESIAN_POINT('Origin',(0.,-2.5,4.5));
#7533=CARTESIAN_POINT('',(-1.,-2.4,4.5));
#7534=CARTESIAN_POINT('Origin',(0.,-2.4,4.5));
#7535=CARTESIAN_POINT('',(-1.,-2.5,4.5));
#7536=CARTESIAN_POINT('',(-1.,-2.5,4.5));
#7537=CARTESIAN_POINT('Origin',(0.,-2.5,4.5));
#7538=CARTESIAN_POINT('Origin',(0.,-2.4,4.5));
#7539=CARTESIAN_POINT('Origin',(0.,-2.5,4.5));
#7776=UNCERTAINTY_MEASURE_WITH_UNIT(LENGTH_MEASURE(0.001),#7807,
'DISTANCE_ACCURACY_VALUE',
'Maximum model space distance between geometric entities at asserted c
onnectivities');
#7782=UNCERTAINTY_MEASURE_WITH_UNIT(LENGTH_MEASURE(0.001),#7807,
'DISTANCE_ACCURACY_VALUE',
'Maximum model space distance between geometric entities at asserted c
onnectivities');
#7800=(
GEOMETRIC_REPRESENTATION_CONTEXT(3)
GLOBAL_UNCERTAINTY_ASSIGNED_CONTEXT((#7776))
GLOBAL_UNIT_ASSIGNED_CONTEXT((#7807,#7809,#7810))
REPRESENTATION_CONTEXT('','3D')
);
#7806=(
GEOMETRIC_REPRESENTATION_CONTEXT(3)
GLOBAL_UNCERTAINTY_ASSIGNED_CONTEXT((#7782))
GLOBAL_UNIT_ASSIGNED_CONTEXT((#7807,#7809,#7810))
REPRESENTATION_CONTEXT('','3D')
);
#7807=(
LENGTH_UNIT()
NAMED_UNIT(*)
SI_UNIT(.CENTI.,.METRE.)
);
#7809=(
NAMED_UNIT(*)
PLANE_ANGLE_UNIT()
SI_UNIT($,.RADIAN.)
);
#7810=(
NAMED_UNIT(*)
SI_UNIT($,.STERADIAN.)
SOLID_ANGLE_UNIT()
);
#7828=SHAPE_DEFINITION_REPRESENTATION(#7856,#7927);
#7856=PRODUCT_DEFINITION_SHAPE('',$,#7951);
#7927=SHAPE_REPRESENTATION('',(#4770),#7800);
#7933=PRODUCT_DEFINITION_CONTEXT('part definition',#8004,'design');
#7951=PRODUCT_DEFINITION('Bracket spacer','Bracket spacer',#7974,#7933);
#7974=PRODUCT_DEFINITION_FORMATION('',$,#8023);
#8004=APPLICATION_CONTEXT(
'Core Data for Automotive Mechanical Design Process');
#8005=PRODUCT_CONTEXT('part definition',#8004,'mechanical');
#8023=PRODUCT('Bracket spacer','Bracket spacer','Bracket spacer',(#8005));
#8064=COLOUR_RGB('Dark Blue',0.08,0.2,0.34);
#8065=FILL_AREA_STYLE_COLOUR('',#8064);
#8066=FILL_AREA_STYLE('',(#8065));
#8067=SURFACE_STYLE_FILL_AREA(#8066);
#8068=SURFACE_SIDE_STYLE('',(#8067));
#8069=SURFACE_STYLE_USAGE(.BOTH.,#8068);
#8070=PRESENTATION_STYLE_ASSIGNMENT((#8069));
ENDSEC;
END-ISO-10303-21;
